ISO-10303-21;
HEADER;
/* Generated by software containing ST-Developer
 * from STEP Tools, Inc. (www.steptools.com) 
 */

FILE_DESCRIPTION(
/* description */ ('Vibration shaker table dummy'),
/* implementation_level */ '2;1');

FILE_NAME(
/* name */ 'M5x14 Cap Screw.step',
/* time_stamp */ '2026-10-27T10:55:14-07:00',
/* author */ (''),
/* organization */ (''),
/* preprocessor_version */ 'ST-DEVELOPER v20.2',
/* originating_system */ 'Autodesk Translation Framework v15.17.0.0',
/* authorisation */ '');

FILE_SCHEMA (('AUTOMOTIVE_DESIGN { 1 0 10303 214 3 1 1 }'));
ENDSEC;

DATA;
#10=MECHANICAL_DESIGN_GEOMETRIC_PRESENTATION_REPRESENTATION('',(#721),#22394);
#567=ORIENTED_CLOSED_SHELL('',*,#9239,.F.);
#570=BREP_WITH_VOIDS('Body1',#9240,(#567));
#575=CONICAL_SURFACE('',#10400,0.4,0.785398163397448);
#576=CONICAL_SURFACE('',#10404,0.41,0.785398163397448);
#577=CONICAL_SURFACE('',#10408,0.26,0.463647609000806);
#629=SHAPE_REPRESENTATION_RELATIONSHIP('SRR','None',#22675,#675);
#675=ADVANCED_BREP_SHAPE_REPRESENTATION('',(#570),#22381);
#721=STYLED_ITEM('',(#22968),#570);
#957=FACE_BOUND('',#2355,.T.);
#1250=PLANE('',#10388);
#1251=PLANE('',#10389);
#1252=PLANE('',#10390);
#1253=PLANE('',#10391);
#1254=PLANE('',#10392);
#1255=PLANE('',#10393);
#1256=PLANE('',#10394);
#1257=PLANE('',#10395);
#1258=PLANE('',#10396);
#1259=PLANE('',#10398);
#1260=PLANE('',#10406);
#1661=FACE_OUTER_BOUND('',#2341,.T.);
#1662=FACE_OUTER_BOUND('',#2342,.T.);
#1663=FACE_OUTER_BOUND('',#2343,.T.);
#1664=FACE_OUTER_BOUND('',#2344,.T.);
#1665=FACE_OUTER_BOUND('',#2345,.T.);
#1666=FACE_OUTER_BOUND('',#2346,.T.);
#1667=FACE_OUTER_BOUND('',#2347,.T.);
#1668=FACE_OUTER_BOUND('',#2348,.T.);
#1669=FACE_OUTER_BOUND('',#2349,.T.);
#1670=FACE_OUTER_BOUND('',#2350,.T.);
#1671=FACE_OUTER_BOUND('',#2351,.T.);
#1672=FACE_OUTER_BOUND('',#2352,.T.);
#1673=FACE_OUTER_BOUND('',#2353,.T.);
#1674=FACE_OUTER_BOUND('',#2354,.T.);
#1675=FACE_OUTER_BOUND('',#2356,.T.);
#1676=FACE_OUTER_BOUND('',#2357,.T.);
#2341=EDGE_LOOP('',(#7634,#7635,#7636,#7637));
#2342=EDGE_LOOP('',(#7638,#7639,#7640,#7641));
#2343=EDGE_LOOP('',(#7642,#7643,#7644,#7645));
#2344=EDGE_LOOP('',(#7646,#7647,#7648,#7649));
#2345=EDGE_LOOP('',(#7650,#7651,#7652,#7653));
#2346=EDGE_LOOP('',(#7654,#7655,#7656,#7657));
#2347=EDGE_LOOP('',(#7658,#7659,#7660,#7661,#7662,#7663));
#2348=EDGE_LOOP('',(#7664,#7665,#7666,#7667,#7668,#7669));
#2349=EDGE_LOOP('',(#7670));
#2350=EDGE_LOOP('',(#7671));
#2351=EDGE_LOOP('',(#7672,#7673,#7674,#7675));
#2352=EDGE_LOOP('',(#7676,#7677,#7678,#7679));
#2353=EDGE_LOOP('',(#7680,#7681,#7682,#7683));
#2354=EDGE_LOOP('',(#7684));
#2355=EDGE_LOOP('',(#7685));
#2356=EDGE_LOOP('',(#7686,#7687,#7688,#7689));
#2357=EDGE_LOOP('',(#7690,#7691,#7692,#7693));
#3038=LINE('',#21244,#3657);
#3039=LINE('',#21246,#3658);
#3040=LINE('',#21248,#3659);
#3041=LINE('',#21249,#3660);
#3042=LINE('',#21252,#3661);
#3043=LINE('',#21254,#3662);
#3044=LINE('',#21255,#3663);
#3045=LINE('',#21258,#3664);
#3046=LINE('',#21260,#3665);
#3047=LINE('',#21261,#3666);
#3048=LINE('',#21264,#3667);
#3049=LINE('',#21266,#3668);
#3050=LINE('',#21267,#3669);
#3051=LINE('',#21270,#3670);
#3052=LINE('',#21272,#3671);
#3053=LINE('',#21273,#3672);
#3054=LINE('',#21275,#3673);
#3055=LINE('',#21276,#3674);
#3056=LINE('',#21288,#3675);
#3057=LINE('',#21292,#3676);
#3058=LINE('',#21296,#3677);
#3059=LINE('',#21303,#3678);
#3060=LINE('',#21305,#3679);
#3657=VECTOR('',#12624,1.);
#3658=VECTOR('',#12625,1.);
#3659=VECTOR('',#12626,1.);
#3660=VECTOR('',#12627,1.);
#3661=VECTOR('',#12630,1.);
#3662=VECTOR('',#12631,1.);
#3663=VECTOR('',#12632,1.);
#3664=VECTOR('',#12635,1.);
#3665=VECTOR('',#12636,1.);
#3666=VECTOR('',#12637,1.);
#3667=VECTOR('',#12640,1.);
#3668=VECTOR('',#12641,1.);
#3669=VECTOR('',#12642,1.);
#3670=VECTOR('',#12645,1.);
#3671=VECTOR('',#12646,1.);
#3672=VECTOR('',#12647,1.);
#3673=VECTOR('',#12650,1.);
#3674=VECTOR('',#12651,1.);
#3675=VECTOR('',#12668,0.4);
#3676=VECTOR('',#12673,0.425);
#3677=VECTOR('',#12678,0.41);
#3678=VECTOR('',#12687,0.26);
#3679=VECTOR('',#12690,0.25);
#4134=CIRCLE('',#10397,0.24505);
#4135=CIRCLE('',#10399,0.375);
#4136=CIRCLE('',#10401,0.425);
#4137=CIRCLE('',#10403,0.425);
#4138=CIRCLE('',#10405,0.395);
#4139=CIRCLE('',#10407,0.27);
#4140=CIRCLE('',#10409,0.24505);
#4829=VERTEX_POINT('',#21242);
#4830=VERTEX_POINT('',#21243);
#4831=VERTEX_POINT('',#21245);
#4832=VERTEX_POINT('',#21247);
#4833=VERTEX_POINT('',#21251);
#4834=VERTEX_POINT('',#21253);
#4835=VERTEX_POINT('',#21257);
#4836=VERTEX_POINT('',#21259);
#4837=VERTEX_POINT('',#21263);
#4838=VERTEX_POINT('',#21265);
#4839=VERTEX_POINT('',#21269);
#4840=VERTEX_POINT('',#21271);
#4841=VERTEX_POINT('',#21280);
#4842=VERTEX_POINT('',#21283);
#4843=VERTEX_POINT('',#21286);
#4844=VERTEX_POINT('',#21290);
#4845=VERTEX_POINT('',#21294);
#4846=VERTEX_POINT('',#21298);
#4847=VERTEX_POINT('',#21301);
#5810=EDGE_CURVE('',#4829,#4830,#3038,.T.);
#5811=EDGE_CURVE('',#4830,#4831,#3039,.T.);
#5812=EDGE_CURVE('',#4831,#4832,#3040,.T.);
#5813=EDGE_CURVE('',#4829,#4832,#3041,.T.);
#5814=EDGE_CURVE('',#4830,#4833,#3042,.T.);
#5815=EDGE_CURVE('',#4833,#4834,#3043,.T.);
#5816=EDGE_CURVE('',#4834,#4831,#3044,.T.);
#5817=EDGE_CURVE('',#4833,#4835,#3045,.T.);
#5818=EDGE_CURVE('',#4835,#4836,#3046,.T.);
#5819=EDGE_CURVE('',#4836,#4834,#3047,.T.);
#5820=EDGE_CURVE('',#4835,#4837,#3048,.T.);
#5821=EDGE_CURVE('',#4837,#4838,#3049,.T.);
#5822=EDGE_CURVE('',#4838,#4836,#3050,.T.);
#5823=EDGE_CURVE('',#4837,#4839,#3051,.T.);
#5824=EDGE_CURVE('',#4839,#4840,#3052,.T.);
#5825=EDGE_CURVE('',#4840,#4838,#3053,.T.);
#5826=EDGE_CURVE('',#4839,#4829,#3054,.T.);
#5827=EDGE_CURVE('',#4832,#4840,#3055,.T.);
#5828=EDGE_CURVE('',#4841,#4841,#4134,.T.);
#5829=EDGE_CURVE('',#4842,#4842,#4135,.T.);
#5830=EDGE_CURVE('',#4843,#4843,#4136,.T.);
#5831=EDGE_CURVE('',#4843,#4842,#3056,.T.);
#5832=EDGE_CURVE('',#4844,#4844,#4137,.T.);
#5833=EDGE_CURVE('',#4844,#4843,#3057,.T.);
#5834=EDGE_CURVE('',#4845,#4845,#4138,.T.);
#5835=EDGE_CURVE('',#4845,#4844,#3058,.T.);
#5836=EDGE_CURVE('',#4846,#4846,#4139,.T.);
#5837=EDGE_CURVE('',#4847,#4847,#4140,.F.);
#5838=EDGE_CURVE('',#4847,#4846,#3059,.T.);
#5839=EDGE_CURVE('',#4841,#4847,#3060,.T.);
#7634=ORIENTED_EDGE('',*,*,#5810,.T.);
#7635=ORIENTED_EDGE('',*,*,#5811,.T.);
#7636=ORIENTED_EDGE('',*,*,#5812,.T.);
#7637=ORIENTED_EDGE('',*,*,#5813,.F.);
#7638=ORIENTED_EDGE('',*,*,#5814,.T.);
#7639=ORIENTED_EDGE('',*,*,#5815,.T.);
#7640=ORIENTED_EDGE('',*,*,#5816,.T.);
#7641=ORIENTED_EDGE('',*,*,#5811,.F.);
#7642=ORIENTED_EDGE('',*,*,#5817,.T.);
#7643=ORIENTED_EDGE('',*,*,#5818,.T.);
#7644=ORIENTED_EDGE('',*,*,#5819,.T.);
#7645=ORIENTED_EDGE('',*,*,#5815,.F.);
#7646=ORIENTED_EDGE('',*,*,#5820,.T.);
#7647=ORIENTED_EDGE('',*,*,#5821,.T.);
#7648=ORIENTED_EDGE('',*,*,#5822,.T.);
#7649=ORIENTED_EDGE('',*,*,#5818,.F.);
#7650=ORIENTED_EDGE('',*,*,#5823,.T.);
#7651=ORIENTED_EDGE('',*,*,#5824,.T.);
#7652=ORIENTED_EDGE('',*,*,#5825,.T.);
#7653=ORIENTED_EDGE('',*,*,#5821,.F.);
#7654=ORIENTED_EDGE('',*,*,#5826,.T.);
#7655=ORIENTED_EDGE('',*,*,#5813,.T.);
#7656=ORIENTED_EDGE('',*,*,#5827,.T.);
#7657=ORIENTED_EDGE('',*,*,#5824,.F.);
#7658=ORIENTED_EDGE('',*,*,#5826,.F.);
#7659=ORIENTED_EDGE('',*,*,#5823,.F.);
#7660=ORIENTED_EDGE('',*,*,#5820,.F.);
#7661=ORIENTED_EDGE('',*,*,#5817,.F.);
#7662=ORIENTED_EDGE('',*,*,#5814,.F.);
#7663=ORIENTED_EDGE('',*,*,#5810,.F.);
#7664=ORIENTED_EDGE('',*,*,#5827,.F.);
#7665=ORIENTED_EDGE('',*,*,#5812,.F.);
#7666=ORIENTED_EDGE('',*,*,#5816,.F.);
#7667=ORIENTED_EDGE('',*,*,#5819,.F.);
#7668=ORIENTED_EDGE('',*,*,#5822,.F.);
#7669=ORIENTED_EDGE('',*,*,#5825,.F.);
#7670=ORIENTED_EDGE('',*,*,#5828,.F.);
#7671=ORIENTED_EDGE('',*,*,#5829,.F.);
#7672=ORIENTED_EDGE('',*,*,#5830,.F.);
#7673=ORIENTED_EDGE('',*,*,#5831,.T.);
#7674=ORIENTED_EDGE('',*,*,#5829,.T.);
#7675=ORIENTED_EDGE('',*,*,#5831,.F.);
#7676=ORIENTED_EDGE('',*,*,#5832,.F.);
#7677=ORIENTED_EDGE('',*,*,#5833,.T.);
#7678=ORIENTED_EDGE('',*,*,#5830,.T.);
#7679=ORIENTED_EDGE('',*,*,#5833,.F.);
#7680=ORIENTED_EDGE('',*,*,#5834,.F.);
#7681=ORIENTED_EDGE('',*,*,#5835,.T.);
#7682=ORIENTED_EDGE('',*,*,#5832,.T.);
#7683=ORIENTED_EDGE('',*,*,#5835,.F.);
#7684=ORIENTED_EDGE('',*,*,#5834,.T.);
#7685=ORIENTED_EDGE('',*,*,#5836,.F.);
#7686=ORIENTED_EDGE('',*,*,#5837,.F.);
#7687=ORIENTED_EDGE('',*,*,#5838,.T.);
#7688=ORIENTED_EDGE('',*,*,#5836,.T.);
#7689=ORIENTED_EDGE('',*,*,#5838,.F.);
#7690=ORIENTED_EDGE('',*,*,#5828,.T.);
#7691=ORIENTED_EDGE('',*,*,#5839,.T.);
#7692=ORIENTED_EDGE('',*,*,#5837,.T.);
#7693=ORIENTED_EDGE('',*,*,#5839,.F.);
#8630=CYLINDRICAL_SURFACE('',#10402,0.425);
#8631=CYLINDRICAL_SURFACE('',#10410,0.24505);
#9026=ADVANCED_FACE('',(#1661),#1250,.F.);
#9027=ADVANCED_FACE('',(#1662),#1251,.F.);
#9028=ADVANCED_FACE('',(#1663),#1252,.F.);
#9029=ADVANCED_FACE('',(#1664),#1253,.F.);
#9030=ADVANCED_FACE('',(#1665),#1254,.F.);
#9031=ADVANCED_FACE('',(#1666),#1255,.F.);
#9032=ADVANCED_FACE('',(#1667),#1256,.F.);
#9033=ADVANCED_FACE('',(#1668),#1257,.F.);
#9034=ADVANCED_FACE('',(#1669),#1258,.F.);
#9035=ADVANCED_FACE('',(#1670),#1259,.T.);
#9036=ADVANCED_FACE('',(#1671),#575,.T.);
#9037=ADVANCED_FACE('',(#1672),#8630,.T.);
#9038=ADVANCED_FACE('',(#1673),#576,.T.);
#9039=ADVANCED_FACE('',(#1674,#957),#1260,.T.);
#9040=ADVANCED_FACE('',(#1675),#577,.T.);
#9041=ADVANCED_FACE('',(#1676),#8631,.T.);
#9239=CLOSED_SHELL('',(#9026,#9027,#9028,#9029,#9030,#9031,#9032,#9033));
#9240=CLOSED_SHELL('',(#9034,#9035,#9036,#9037,#9038,#9039,#9040,#9041));
#10387=AXIS2_PLACEMENT_3D('',#21240,#12620,#12621);
#10388=AXIS2_PLACEMENT_3D('',#21241,#12622,#12623);
#10389=AXIS2_PLACEMENT_3D('',#21250,#12628,#12629);
#10390=AXIS2_PLACEMENT_3D('',#21256,#12633,#12634);
#10391=AXIS2_PLACEMENT_3D('',#21262,#12638,#12639);
#10392=AXIS2_PLACEMENT_3D('',#21268,#12643,#12644);
#10393=AXIS2_PLACEMENT_3D('',#21274,#12648,#12649);
#10394=AXIS2_PLACEMENT_3D('',#21277,#12652,#12653);
#10395=AXIS2_PLACEMENT_3D('',#21278,#12654,#12655);
#10396=AXIS2_PLACEMENT_3D('',#21279,#12656,#12657);
#10397=AXIS2_PLACEMENT_3D('',#21281,#12658,#12659);
#10398=AXIS2_PLACEMENT_3D('',#21282,#12660,#12661);
#10399=AXIS2_PLACEMENT_3D('',#21284,#12662,#12663);
#10400=AXIS2_PLACEMENT_3D('',#21285,#12664,#12665);
#10401=AXIS2_PLACEMENT_3D('',#21287,#12666,#12667);
#10402=AXIS2_PLACEMENT_3D('',#21289,#12669,#12670);
#10403=AXIS2_PLACEMENT_3D('',#21291,#12671,#12672);
#10404=AXIS2_PLACEMENT_3D('',#21293,#12674,#12675);
#10405=AXIS2_PLACEMENT_3D('',#21295,#12676,#12677);
#10406=AXIS2_PLACEMENT_3D('',#21297,#12679,#12680);
#10407=AXIS2_PLACEMENT_3D('',#21299,#12681,#12682);
#10408=AXIS2_PLACEMENT_3D('',#21300,#12683,#12684);
#10409=AXIS2_PLACEMENT_3D('',#21302,#12685,#12686);
#10410=AXIS2_PLACEMENT_3D('',#21304,#12688,#12689);
#12620=DIRECTION('axis',(0.,0.,1.));
#12621=DIRECTION('refdir',(1.,0.,0.));
#12622=DIRECTION('center_axis',(0.866025403784439,0.,-0.5));
#12623=DIRECTION('ref_axis',(0.5,0.,0.866025403784439));
#12624=DIRECTION('',(-0.5,0.,-0.866025403784439));
#12625=DIRECTION('',(0.,-1.,0.));
#12626=DIRECTION('',(0.5,0.,0.866025403784439));
#12627=DIRECTION('',(0.,-1.,0.));
#12628=DIRECTION('center_axis',(1.20185167898973E-16,0.,-1.));
#12629=DIRECTION('ref_axis',(1.,0.,1.20185167898973E-16));
#12630=DIRECTION('',(-1.,0.,-1.20185167898973E-16));
#12631=DIRECTION('',(0.,-1.,0.));
#12632=DIRECTION('',(1.,0.,1.20185167898973E-16));
#12633=DIRECTION('center_axis',(-0.866025403784439,0.,-0.5));
#12634=DIRECTION('ref_axis',(0.5,0.,-0.866025403784439));
#12635=DIRECTION('',(-0.5,0.,0.866025403784439));
#12636=DIRECTION('',(0.,-1.,0.));
#12637=DIRECTION('',(0.5,0.,-0.866025403784439));
#12638=DIRECTION('center_axis',(-0.866025403784439,0.,0.5));
#12639=DIRECTION('ref_axis',(-0.5,0.,-0.866025403784439));
#12640=DIRECTION('',(0.5,0.,0.866025403784439));
#12641=DIRECTION('',(0.,-1.,0.));
#12642=DIRECTION('',(-0.5,0.,-0.866025403784439));
#12643=DIRECTION('center_axis',(-2.40370335797945E-16,0.,1.));
#12644=DIRECTION('ref_axis',(-1.,0.,-2.40370335797945E-16));
#12645=DIRECTION('',(1.,0.,2.40370335797945E-16));
#12646=DIRECTION('',(0.,-1.,0.));
#12647=DIRECTION('',(-1.,0.,-2.40370335797945E-16));
#12648=DIRECTION('center_axis',(0.866025403784439,0.,0.5));
#12649=DIRECTION('ref_axis',(-0.5,0.,0.866025403784439));
#12650=DIRECTION('',(0.5,0.,-0.866025403784439));
#12651=DIRECTION('',(-0.5,0.,0.866025403784439));
#12652=DIRECTION('center_axis',(0.,1.,0.));
#12653=DIRECTION('ref_axis',(1.,0.,0.));
#12654=DIRECTION('center_axis',(0.,-1.,0.));
#12655=DIRECTION('ref_axis',(0.,0.,-1.));
#12656=DIRECTION('center_axis',(0.,1.,0.));
#12657=DIRECTION('ref_axis',(1.,0.,0.));
#12658=DIRECTION('center_axis',(0.,1.,0.));
#12659=DIRECTION('ref_axis',(1.,0.,0.));
#12660=DIRECTION('center_axis',(0.,1.,0.));
#12661=DIRECTION('ref_axis',(0.,0.,1.));
#12662=DIRECTION('center_axis',(0.,-1.,0.));
#12663=DIRECTION('ref_axis',(1.,0.,0.));
#12664=DIRECTION('center_axis',(0.,-1.,0.));
#12665=DIRECTION('ref_axis',(1.,0.,0.));
#12666=DIRECTION('center_axis',(0.,-1.,0.));
#12667=DIRECTION('ref_axis',(1.,0.,0.));
#12668=DIRECTION('',(0.707106781186548,0.707106781186547,8.65956056235493E-17));
#12669=DIRECTION('center_axis',(0.,-1.,0.));
#12670=DIRECTION('ref_axis',(1.,0.,0.));
#12671=DIRECTION('center_axis',(0.,-1.,0.));
#12672=DIRECTION('ref_axis',(1.,0.,0.));
#12673=DIRECTION('',(0.,1.,0.));
#12674=DIRECTION('center_axis',(0.,1.,0.));
#12675=DIRECTION('ref_axis',(1.,0.,0.));
#12676=DIRECTION('center_axis',(0.,-1.,0.));
#12677=DIRECTION('ref_axis',(1.,0.,0.));
#12678=DIRECTION('',(-0.707106781186547,0.707106781186548,-8.65956056235493E-17));
#12679=DIRECTION('center_axis',(0.,-1.,0.));
#12680=DIRECTION('ref_axis',(0.,0.,-1.));
#12681=DIRECTION('center_axis',(0.,-1.,0.));
#12682=DIRECTION('ref_axis',(1.,0.,0.));
#12683=DIRECTION('center_axis',(0.,1.,0.));
#12684=DIRECTION('ref_axis',(1.,0.,0.));
#12685=DIRECTION('center_axis',(0.,1.,0.));
#12686=DIRECTION('ref_axis',(1.,0.,0.));
#12687=DIRECTION('',(-0.447213595499958,0.894427190999916,-5.47678698264203E-17));
#12688=DIRECTION('center_axis',(0.,-1.,0.));
#12689=DIRECTION('ref_axis',(1.,0.,0.));
#12690=DIRECTION('',(0.,1.,0.));
#21240=CARTESIAN_POINT('',(0.,0.,0.));
#21241=CARTESIAN_POINT('Origin',(0.115470053837925,-0.5,-0.2));
#21242=CARTESIAN_POINT('',(0.23094010767585,-0.5,0.));
#21243=CARTESIAN_POINT('',(0.115470053837925,-0.5,-0.2));
#21244=CARTESIAN_POINT('',(0.23094010767585,-0.5,0.));
#21245=CARTESIAN_POINT('',(0.115470053837925,-0.8,-0.2));
#21246=CARTESIAN_POINT('',(0.115470053837925,-0.5,-0.2));
#21247=CARTESIAN_POINT('',(0.23094010767585,-0.8,0.));
#21248=CARTESIAN_POINT('',(0.23094010767585,-0.8,0.));
#21249=CARTESIAN_POINT('',(0.23094010767585,-0.5,0.));
#21250=CARTESIAN_POINT('Origin',(-0.115470053837925,-0.5,-0.2));
#21251=CARTESIAN_POINT('',(-0.115470053837925,-0.5,-0.2));
#21252=CARTESIAN_POINT('',(0.115470053837925,-0.5,-0.2));
#21253=CARTESIAN_POINT('',(-0.115470053837925,-0.8,-0.2));
#21254=CARTESIAN_POINT('',(-0.115470053837925,-0.5,-0.2));
#21255=CARTESIAN_POINT('',(0.115470053837925,-0.8,-0.2));
#21256=CARTESIAN_POINT('Origin',(-0.23094010767585,-0.5,-2.77555756156289E-17));
#21257=CARTESIAN_POINT('',(-0.23094010767585,-0.5,-2.82820063659975E-17));
#21258=CARTESIAN_POINT('',(-0.115470053837925,-0.5,-0.2));
#21259=CARTESIAN_POINT('',(-0.23094010767585,-0.8,-2.77555756156289E-17));
#21260=CARTESIAN_POINT('',(-0.23094010767585,-0.5,-2.82820063659975E-17));
#21261=CARTESIAN_POINT('',(-0.115470053837925,-0.8,-0.2));
#21262=CARTESIAN_POINT('Origin',(-0.115470053837925,-0.5,0.2));
#21263=CARTESIAN_POINT('',(-0.115470053837925,-0.5,0.2));
#21264=CARTESIAN_POINT('',(-0.23094010767585,-0.5,-2.82820063659975E-17));
#21265=CARTESIAN_POINT('',(-0.115470053837925,-0.8,0.2));
#21266=CARTESIAN_POINT('',(-0.115470053837925,-0.5,0.2));
#21267=CARTESIAN_POINT('',(-0.23094010767585,-0.8,-2.82820063659975E-17));
#21268=CARTESIAN_POINT('Origin',(0.115470053837925,-0.5,0.2));
#21269=CARTESIAN_POINT('',(0.115470053837925,-0.5,0.2));
#21270=CARTESIAN_POINT('',(-0.115470053837925,-0.5,0.2));
#21271=CARTESIAN_POINT('',(0.115470053837925,-0.8,0.2));
#21272=CARTESIAN_POINT('',(0.115470053837925,-0.5,0.2));
#21273=CARTESIAN_POINT('',(-0.115470053837925,-0.8,0.2));
#21274=CARTESIAN_POINT('Origin',(0.23094010767585,-0.5,0.));
#21275=CARTESIAN_POINT('',(0.115470053837925,-0.5,0.2));
#21276=CARTESIAN_POINT('',(0.115470053837925,-0.8,0.2));
#21277=CARTESIAN_POINT('Origin',(0.,-0.5,0.));
#21278=CARTESIAN_POINT('Origin',(0.,-0.8,0.));
#21279=CARTESIAN_POINT('Origin',(0.,-1.4,0.));
#21280=CARTESIAN_POINT('',(-0.24505,-1.4,3.00099698131059E-17));
#21281=CARTESIAN_POINT('Origin',(0.,-1.4,0.));
#21282=CARTESIAN_POINT('Origin',(0.375,0.5,0.));
#21283=CARTESIAN_POINT('',(-0.375,0.5,-4.59242549680257E-17));
#21284=CARTESIAN_POINT('Origin',(0.,0.5,0.));
#21285=CARTESIAN_POINT('Origin',(0.,0.475,0.));
#21286=CARTESIAN_POINT('',(-0.425,0.45,-5.20474889637625E-17));
#21287=CARTESIAN_POINT('Origin',(0.,0.45,0.));
#21288=CARTESIAN_POINT('',(-0.4,0.475,-4.89858719658941E-17));
#21289=CARTESIAN_POINT('Origin',(0.,0.24,0.));
#21290=CARTESIAN_POINT('',(-0.425,0.0299999999999998,-5.20474889637625E-17));
#21291=CARTESIAN_POINT('Origin',(0.,0.0299999999999998,0.));
#21292=CARTESIAN_POINT('',(-0.425,0.24,-5.20474889637625E-17));
#21293=CARTESIAN_POINT('Origin',(0.,0.0150000000000001,0.));
#21294=CARTESIAN_POINT('',(-0.395,4.85722573273506E-17,-4.83735485663204E-17));
#21295=CARTESIAN_POINT('Origin',(0.,0.,0.));
#21296=CARTESIAN_POINT('',(-0.41,0.0150000000000001,-5.02105187650415E-17));
#21297=CARTESIAN_POINT('Origin',(0.27,0.,0.));
#21298=CARTESIAN_POINT('',(-0.27,0.,-3.30654635769785E-17));
#21299=CARTESIAN_POINT('Origin',(0.,0.,0.));
#21300=CARTESIAN_POINT('Origin',(0.,-0.02,0.));
#21301=CARTESIAN_POINT('',(-0.24505,-0.0498999999999999,3.00099698131059E-17));
#21302=CARTESIAN_POINT('Origin',(0.,-0.0498999999999999,0.));
#21303=CARTESIAN_POINT('',(-0.26,-0.02,-3.18408167778312E-17));
#21304=CARTESIAN_POINT('Origin',(0.,-0.995,0.));
#21305=CARTESIAN_POINT('',(-0.24505,-0.995,-3.00099698131059E-17));
#22330=UNCERTAINTY_MEASURE_WITH_UNIT(LENGTH_MEASURE(0.001),#22395,
'DISTANCE_ACCURACY_VALUE',
'Maximum model space distance between geometric entities at asserted c
onnectivities');
#22343=UNCERTAINTY_MEASURE_WITH_UNIT(LENGTH_MEASURE(0.001),#22395,
'DISTANCE_ACCURACY_VALUE',
'Maximum model space distance between geometric entities at asserted c
onnectivities');
#22381=(
GEOMETRIC_REPRESENTATION_CONTEXT(3)
GLOBAL_UNCERTAINTY_ASSIGNED_CONTEXT((#22330))
GLOBAL_UNIT_ASSIGNED_CONTEXT((#22395,#22397,#22398))
REPRESENTATION_CONTEXT('','3D')
);
#22394=(
GEOMETRIC_REPRESENTATION_CONTEXT(3)
GLOBAL_UNCERTAINTY_ASSIGNED_CONTEXT((#22343))
GLOBAL_UNIT_ASSIGNED_CONTEXT((#22395,#22397,#22398))
REPRESENTATION_CONTEXT('','3D')
);
#22395=(
LENGTH_UNIT()
NAMED_UNIT(*)
SI_UNIT(.CENTI.,.METRE.)
);
#22397=(
NAMED_UNIT(*)
PLANE_ANGLE_UNIT()
SI_UNIT($,.RADIAN.)
);
#22398=(
NAMED_UNIT(*)
SI_UNIT($,.STERADIAN.)
SOLID_ANGLE_UNIT()
);
#22436=SHAPE_DEFINITION_REPRESENTATION(#22486,#22675);
#22486=PRODUCT_DEFINITION_SHAPE('',$,#22726);
#22675=SHAPE_REPRESENTATION('',(#10387),#22381);
#22688=PRODUCT_DEFINITION_CONTEXT('part definition',#22840,'design');
#22726=PRODUCT_DEFINITION('M5x14 Cap Screw','M5x14 Cap Screw',#22776,#22688);
#22776=PRODUCT_DEFINITION_FORMATION('',$,#22879);
#22840=APPLICATION_CONTEXT(
'Core Data for Automotive Mechanical Design Process');
#22841=PRODUCT_CONTEXT('part definition',#22840,'mechanical');
#22879=PRODUCT('M5x14 Cap Screw','M5x14 Cap Screw','M5x14 Cap Screw',(#22841));
#22962=COLOUR_RGB('Black',0.12,0.14,0.17);
#22963=FILL_AREA_STYLE_COLOUR('',#22962);
#22964=FILL_AREA_STYLE('',(#22963));
#22965=SURFACE_STYLE_FILL_AREA(#22964);
#22966=SURFACE_SIDE_STYLE('',(#22965));
#22967=SURFACE_STYLE_USAGE(.BOTH.,#22966);
#22968=PRESENTATION_STYLE_ASSIGNMENT((#22967));
ENDSEC;
END-ISO-10303-21;
